ISO-10303-21;
HEADER;
FILE_DESCRIPTION (('STEP AP214'),
    '1' );
FILE_NAME ('Screw 8.step',
    '2026-10-26T17:37:43',
    ( '' ),
    ( '' ),
    'SwSTEP 2.0',
    'SolidWorks 2024',
    '' );
FILE_SCHEMA (( 'AUTOMOTIVE_DESIGN' ));
ENDSEC;

DATA;
#19=LINE ( 'NONE', #12552, #15858 ) ;
#38=ORIENTED_EDGE ( 'NONE', *, *, #8360, .F. ) ;
#47=EDGE_CURVE ( 'NONE', #7611, #9417, #20192, .T. ) ;
#64=DIRECTION ( 'NONE',  ( 0.000000000000000000, -2.336881798971000105E-14, 1.000000000000000000 ) ) ;
#106=CARTESIAN_POINT ( 'NONE',  ( 139.6999999999999886, -3659.504999999999654, 2272.030000000000200 ) ) ;
#146=CARTESIAN_POINT ( 'NONE',  ( 139.7000000000063835, -3656.812599999938357, 2239.391000000000076 ) ) ;
#186=CARTESIAN_POINT ( 'NONE',  ( 139.6999999999999886, -3659.504999999999654, 2239.391000000000076 ) ) ;
#229=DIRECTION ( 'NONE',  ( 0.000000000000000000, 0.000000000000000000, -1.000000000000000000 ) ) ;
#248=EDGE_CURVE ( 'NONE', #8112, #12304, #9278, .T. ) ;
#269=EDGE_CURVE ( 'NONE', #14110, #7171, #20694, .T. ) ;
#276=DIRECTION ( 'NONE',  ( -3.561520347316999955E-13, -6.475491540576999783E-13, 1.000000000000000000 ) ) ;
#282=ORIENTED_EDGE ( 'NONE', *, *, #8857, .F. ) ;
#326=FACE_OUTER_BOUND ( 'NONE', #6088, .T. ) ;
#341=EDGE_CURVE ( 'NONE', #9417, #7352, #19, .T. ) ;
#364=DIRECTION ( 'NONE',  ( 1.298916404569000195E-12, -1.000000000000000000, 0.000000000000000000 ) ) ;
#420=ORIENTED_EDGE ( 'NONE', *, *, #341, .F. ) ;
#467=VECTOR ( 'NONE', #18120, 1000.000000000000000 ) ;
#506=ORIENTED_EDGE ( 'NONE', *, *, #6294, .F. ) ;
#524=AXIS2_PLACEMENT_3D ( 'NONE', #11468, #8077, #15225 ) ;
#529=DIRECTION ( 'NONE',  ( 0.000000000000000000, 2.336881798971000105E-14, -1.000000000000000000 ) ) ;
#546=VECTOR ( 'NONE', #10969, 1000.000000000000114 ) ;
#554=DIRECTION ( 'NONE',  ( 0.000000000000000000, 0.000000000000000000, 1.000000000000000000 ) ) ;
#565=VERTEX_POINT ( 'NONE', #2407 ) ;
#641=AXIS2_PLACEMENT_3D ( 'NONE', #16401, #9374, #7492 ) ;
#685=ORIENTED_EDGE ( 'NONE', *, *, #9708, .F. ) ;
#695=DIRECTION ( 'NONE',  ( -2.848935406719999894E-12, 1.000000000000000000, 2.336881798978000141E-14 ) ) ;
#774=EDGE_CURVE ( 'NONE', #11858, #19931, #1566, .T. ) ;
#788=ORIENTED_EDGE ( 'NONE', *, *, #18877, .T. ) ;
#836=AXIS2_PLACEMENT_3D ( 'NONE', #12560, #7289, #21924 ) ;
#891=AXIS2_PLACEMENT_3D ( 'NONE', #11198, #9334, #9445 ) ;
#911=PLANE ( 'NONE',  #6522 ) ;
#953=VECTOR ( 'NONE', #3074, 1000.000000000000114 ) ;
#962=DIRECTION ( 'NONE',  ( -0.8660254037825932949, -0.5000000000031962211, 5.608020032303961777E-12 ) ) ;
#970=PLANE ( 'NONE',  #17126 ) ;
#1003=AXIS2_PLACEMENT_3D ( 'NONE', #2063, #21859, #16238 ) ;
#1044=VERTEX_POINT ( 'NONE', #13265 ) ;
#1077=CARTESIAN_POINT ( 'NONE',  ( 137.3683132029851208, -3660.851200000049630, 2239.391000000000076 ) ) ;
#1087=ORIENTED_EDGE ( 'NONE', *, *, #5302, .F. ) ;
#1092=VERTEX_POINT ( 'NONE', #9978 ) ;
#1099=EDGE_CURVE ( 'NONE', #11125, #20633, #16892, .T. ) ;
#1247=CARTESIAN_POINT ( 'NONE',  ( 139.6999999999999886, -3662.637340904999746, 2239.009999999999764 ) ) ;
#1269=ORIENTED_EDGE ( 'NONE', *, *, #2702, .F. ) ;
#1438=VERTEX_POINT ( 'NONE', #13237 ) ;
#1556=CARTESIAN_POINT ( 'NONE',  ( 142.0316867971999955, -3660.851200000000063, 2242.820000000000164 ) ) ;
#1566=LINE ( 'NONE', #21266, #17250 ) ;
#1613=DIRECTION ( 'NONE',  ( 1.000000000000000000, 5.432398939370942693E-28, -2.324635735433000053E-14 ) ) ;
#1628=EDGE_CURVE ( 'NONE', #19068, #19181, #15812, .T. ) ;
#1663=EDGE_CURVE ( 'NONE', #18199, #7611, #8000, .T. ) ;
#1665=CARTESIAN_POINT ( 'NONE',  ( 137.3683132029851208, -3660.851200000049630, 2239.391000000000076 ) ) ;
#1678=ORIENTED_EDGE ( 'NONE', *, *, #2220, .F. ) ;
#1714=PRODUCT_DEFINITION_SHAPE ( 'NONE', 'NONE',  #22959 ) ;
#1740=TOROIDAL_SURFACE ( 'NONE', #17825, 1.905000000000000027, 1.270000000000000018 ) ;
#1753=ORIENTED_EDGE ( 'NONE', *, *, #9708, .T. ) ;
#1789=VECTOR ( 'NONE', #6465, 1000.000000000000000 ) ;
#1792=ORIENTED_EDGE ( 'NONE', *, *, #6294, .T. ) ;
#1821=CARTESIAN_POINT ( 'NONE',  ( 139.6999999999999886, -3659.504999999999654, 2272.030000000000200 ) ) ;
#1855=DIRECTION ( 'NONE',  ( -0.5000000000031962211, 0.8660254037825932949, 0.000000000000000000 ) ) ;
#1900=CARTESIAN_POINT ( 'NONE',  ( 137.2104978356082938, -3660.942314744984742, 2239.009999999967931 ) ) ;
#2005=CARTESIAN_POINT ( 'NONE',  ( 139.6999999999999886, -3662.197400000000016, 2242.820000000000164 ) ) ;
#2006=CARTESIAN_POINT ( 'NONE',  ( 139.7000000001000046, -3656.812599999999748, 2242.820000000000164 ) ) ;
#2063=CARTESIAN_POINT ( 'NONE',  ( 139.6999999999999886, -3659.504999999999654, 2239.009999999999764 ) ) ;
#2103=CYLINDRICAL_SURFACE ( 'NONE', #8446, 3.175000000000149925 ) ;
#2116=CYLINDRICAL_SURFACE ( 'NONE', #641, 0.3809999999999924558 ) ;
#2120=VERTEX_POINT ( 'NONE', #6424 ) ;
#2140=VECTOR ( 'NONE', #276, 1000.000000000000000 ) ;
#2141=CARTESIAN_POINT ( 'NONE',  ( 137.3683132029000262, -3658.158799999999701, 2242.820000000000164 ) ) ;
#2151=EDGE_LOOP ( 'NONE', ( #20970, #18599, #20729, #22992 ) ) ;
#2165=ORIENTED_EDGE ( 'NONE', *, *, #17307, .F. ) ;
#2204=CARTESIAN_POINT ( 'NONE',  ( 134.6199999999999761, -3659.504999999999654, 2245.359999999999673 ) ) ;
#2220=EDGE_CURVE ( 'NONE', #8112, #7611, #3358, .T. ) ;
#2234=ORIENTED_EDGE ( 'NONE', *, *, #13511, .T. ) ;
#2257=( GEOMETRIC_REPRESENTATION_CONTEXT ( 3 ) GLOBAL_UNCERTAINTY_ASSIGNED_CONTEXT ( ( #16741 ) ) GLOBAL_UNIT_ASSIGNED_CONTEXT ( ( #21126, #3419, #23094 ) ) REPRESENTATION_CONTEXT ( 'NONE', 'WORKASPACE' ) );
#2283=ORIENTED_EDGE ( 'NONE', *, *, #19752, .T. ) ;
#2315=DIRECTION ( 'NONE',  ( 0.000000000000000000, -1.000000000000000000, 0.000000000000000000 ) ) ;
#2317=FACE_OUTER_BOUND ( 'NONE', #8167, .T. ) ;
#2348=VERTEX_POINT ( 'NONE', #2953 ) ;
#2373=ADVANCED_FACE ( 'NONE', ( #18580 ), #22199, .T. ) ;
#2407=CARTESIAN_POINT ( 'NONE',  ( 145.1609999999999729, -3659.504999999999654, 2244.978999999999814 ) ) ;
#2585=ORIENTED_EDGE ( 'NONE', *, *, #15117, .F. ) ;
#2606=CARTESIAN_POINT ( 'NONE',  ( 0.000000000000000000, 0.000000000000000000, 0.000000000000000000 ) ) ;
#2652=DIRECTION ( 'NONE',  ( 0.8660254037820102058, -0.5000000000042060799, 0.000000000000000000 ) ) ;
#2673=FACE_OUTER_BOUND ( 'NONE', #17168, .T. ) ;
#2702=EDGE_CURVE ( 'NONE', #13348, #21028, #9467, .T. ) ;
#2735=CARTESIAN_POINT ( 'NONE',  ( 144.7800000000000011, -3659.504999999999654, 2245.359999999999673 ) ) ;
#2766=CARTESIAN_POINT ( 'NONE',  ( 137.3683132029000262, -3658.158799999999701, 2242.820000000000164 ) ) ;
#2811=AXIS2_PLACEMENT_3D ( 'NONE', #21696, #7285, #12784 ) ;
#2849=CIRCLE ( 'NONE', #19321, 0.3809999999999647002 ) ;
#2917=AXIS2_PLACEMENT_3D ( 'NONE', #14073, #16057, #10898 ) ;
#2949=EDGE_LOOP ( 'NONE', ( #14778, #12228 ) ) ;
#2951=ORIENTED_EDGE ( 'NONE', *, *, #13866, .T. ) ;
#2953=CARTESIAN_POINT ( 'NONE',  ( 137.3683132029000262, -3658.158799999999701, 2242.820000000000164 ) ) ;
#2959=ADVANCED_FACE ( 'NONE', ( #21217 ), #22292, .T. ) ;
#3016=CARTESIAN_POINT ( 'NONE',  ( 139.6999999999999886, -3659.504999999999654, 2245.359999999999673 ) ) ;
#3051=EDGE_CURVE ( 'NONE', #5217, #7352, #10307, .T. ) ;
#3074=DIRECTION ( 'NONE',  ( -0.8660254037839142383, -0.5000000000009082735, 0.000000000000000000 ) ) ;
#3089=ORIENTED_EDGE ( 'NONE', *, *, #20301, .F. ) ;
#3169=ORIENTED_EDGE ( 'NONE', *, *, #10690, .T. ) ;
#3189=CARTESIAN_POINT ( 'NONE',  ( 139.7000000001000046, -3656.372659094999563, 2239.009999999999764 ) ) ;
#3224=VECTOR ( 'NONE', #15591, 1000.000000000000000 ) ;
#3231=FACE_OUTER_BOUND ( 'NONE', #15368, .T. ) ;
#3334=( BOUNDED_CURVE ( )  B_SPLINE_CURVE ( 3, ( #19949, #21701, #11035, #7520 ),
 .UNSPECIFIED., .F., .T. ) 
 B_SPLINE_CURVE_WITH_KNOTS ( ( 4, 4 ),
 ( 3.673835071120113713E-14, 1.570796326419416467 ),
 .UNSPECIFIED. ) 
 CURVE ( )  GEOMETRIC_REPRESENTATION_ITEM ( )  RATIONAL_B_SPLINE_CURVE ( ( 1.000000000000000000, 0.8047378542128751366, 0.8047378542128751366, 1.000000000000000000 ) ) 
 REPRESENTATION_ITEM ( '' )  );
#3344=DIRECTION ( 'NONE',  ( 0.000000000000000000, 0.000000000000000000, 1.000000000000000000 ) ) ;
#3358=LINE ( 'NONE', #18006, #467 ) ;
#3377=ORIENTED_EDGE ( 'NONE', *, *, #15866, .F. ) ;
#3419=( NAMED_UNIT ( * ) PLANE_ANGLE_UNIT ( ) SI_UNIT ( $, .RADIAN. ) );
#3428=ADVANCED_FACE ( 'NONE', ( #22906 ), #8500, .T. ) ;
#3494=ORIENTED_EDGE ( 'NONE', *, *, #19752, .F. ) ;
#3496=AXIS2_PLACEMENT_3D ( 'NONE', #21078, #13929, #10635 ) ;
#3500=ORIENTED_EDGE ( 'NONE', *, *, #1628, .T. ) ;
#3509=EDGE_CURVE ( 'NONE', #1092, #8539, #3621, .T. ) ;
#3570=AXIS2_PLACEMENT_3D ( 'NONE', #22507, #17348, #10448 ) ;
#3621=CIRCLE ( 'NONE', #1003, 5.080000000000000959 ) ;
#3640=EDGE_CURVE ( 'NONE', #1044, #18165, #20483, .T. ) ;
#3656=DIRECTION ( 'NONE',  ( 0.000000000000000000, -1.000000000000000000, 0.000000000000000000 ) ) ;
#3670=EDGE_CURVE ( 'NONE', #7352, #11125, #6644, .T. ) ;
#3791=LINE ( 'NONE', #18207, #6996 ) ;
#3794=DIRECTION ( 'NONE',  ( 0.000000000000000000, -1.000000000000000000, 0.000000000000000000 ) ) ;
#3802=VERTEX_POINT ( 'NONE', #20402 ) ;
#3877=AXIS2_PLACEMENT_3D ( 'NONE', #21459, #16411, #5766 ) ;
#3942=CARTESIAN_POINT ( 'NONE',  ( 142.0316867971999955, -3658.158799999999701, 2242.820000000000164 ) ) ;
#3990=EDGE_CURVE ( 'NONE', #19181, #7611, #5048, .T. ) ;
#4046=CARTESIAN_POINT ( 'NONE',  ( 142.0316867971266390, -3660.851200000091012, 2239.391000000000076 ) ) ;
#4052=CARTESIAN_POINT ( 'NONE',  ( 139.6999999999999886, -3662.197400000000016, 2242.820000000000164 ) ) ;
#4117=ORIENTED_EDGE ( 'NONE', *, *, #13511, .F. ) ;
#4223=EDGE_CURVE ( 'NONE', #13513, #19068, #5616, .T. ) ;
#4273=LINE ( 'NONE', #9662, #12167 ) ;
#4299=FACE_OUTER_BOUND ( 'NONE', #20323, .T. ) ;
#4357=DIRECTION ( 'NONE',  ( -2.324635735433000053E-14, 0.000000000000000000, -1.000000000000000000 ) ) ;
#4373=VECTOR ( 'NONE', #962, 1000.000000000000000 ) ;
#4382=CARTESIAN_POINT ( 'NONE',  ( 144.7800000000000011, -3659.504999999999654, 2239.391000000000076 ) ) ;
#4387=DIRECTION ( 'NONE',  ( 0.000000000000000000, 0.000000000000000000, -1.000000000000000000 ) ) ;
#4444=EDGE_LOOP ( 'NONE', ( #282, #12706, #8347, #4918 ) ) ;
#4522=FACE_OUTER_BOUND ( 'NONE', #16707, .T. ) ;
#4552=EDGE_LOOP ( 'NONE', ( #10248, #7218 ) ) ;
#4592=ORIENTED_EDGE ( 'NONE', *, *, #2220, .T. ) ;
#4603=AXIS2_PLACEMENT_3D ( 'NONE', #8502, #5574, #17868 ) ;
#4607=CARTESIAN_POINT ( 'NONE',  ( 139.6999999999999886, -3659.504999999999654, 2245.359999999999673 ) ) ;
#4609=DIRECTION ( 'NONE',  ( 0.000000000000000000, -1.000000000000000000, 0.000000000000000000 ) ) ;
#4642=DIRECTION ( 'NONE',  ( 0.8660254037842058938, 0.5000000000004030110, -5.443078266503040078E-12 ) ) ;
#4662=CIRCLE ( 'NONE', #10655, 5.460999999999938126 ) ;
#4667=DIRECTION ( 'NONE',  ( 0.000000000000000000, 0.000000000000000000, -1.000000000000000000 ) ) ;
#4731=DIRECTION ( 'NONE',  ( -2.324635735433000053E-14, 0.000000000000000000, -1.000000000000000000 ) ) ;
#4732=VERTEX_POINT ( 'NONE', #2204 ) ;
#4829=CIRCLE ( 'NONE', #8959, 1.904999999999823501 ) ;
#4846=ORIENTED_EDGE ( 'NONE', *, *, #4223, .T. ) ;
#4866=ORIENTED_EDGE ( 'NONE', *, *, #774, .T. ) ;
#4903=FACE_OUTER_BOUND ( 'NONE', #8047, .T. ) ;
#4918=ORIENTED_EDGE ( 'NONE', *, *, #6805, .F. ) ;
#5008=EDGE_CURVE ( 'NONE', #21028, #15441, #4829, .T. ) ;
#5048=LINE ( 'NONE', #13725, #1789 ) ;
#5063=ORIENTED_EDGE ( 'NONE', *, *, #15852, .F. ) ;
#5065=CARTESIAN_POINT ( 'NONE',  ( 142.4126867972053674, -3661.071170452545175, 2239.009999999999764 ) ) ;
#5080=PRODUCT ( 'Screw 8', 'Screw 8', '', ( #9228 ) ) ;
#5122=CARTESIAN_POINT ( 'NONE',  ( 139.6999999999999886, -3659.504999999999654, 2270.760000000000218 ) ) ;
#5126=CARTESIAN_POINT ( 'NONE',  ( 142.4126867973298545, -3657.938829547075329, 2239.009999999999764 ) ) ;
#5193=CARTESIAN_POINT ( 'NONE',  ( 134.6199999999999761, -3659.504999999999654, 2239.009999999999764 ) ) ;
#5206=ORIENTED_EDGE ( 'NONE', *, *, #1663, .T. ) ;
#5217=VERTEX_POINT ( 'NONE', #21631 ) ;
#5218=FACE_OUTER_BOUND ( 'NONE', #2151, .T. ) ;
#5270=ADVANCED_FACE ( 'NONE', ( #10432, #18558 ), #970, .F. ) ;
#5292=ORIENTED_EDGE ( 'NONE', *, *, #21685, .T. ) ;
#5302=EDGE_CURVE ( 'NONE', #7171, #1092, #12279, .T. ) ;
#5319=AXIS2_PLACEMENT_3D ( 'NONE', #8240, #8482, #13507 ) ;
#5332=SHAPE_REPRESENTATION ( 'Screw 8', ( #5611 ), #6759 ) ;
#5435=EDGE_CURVE ( 'NONE', #18165, #8539, #13035, .T. ) ;
#5490=ORIENTED_EDGE ( 'NONE', *, *, #16082, .T. ) ;
#5524=CARTESIAN_POINT ( 'NONE',  ( 142.1895021644337191, -3660.942314744887426, 2239.010000000037508 ) ) ;
#5550=DIRECTION ( 'NONE',  ( -1.206643234470999950E-12, 1.000000000000000000, 0.000000000000000000 ) ) ;
#5574=DIRECTION ( 'NONE',  ( 1.000000000000000000, 0.000000000000000000, 0.000000000000000000 ) ) ;
#5611=AXIS2_PLACEMENT_3D ( 'NONE', #2606, #9751, #7545 ) ;
#5616=( BOUNDED_CURVE ( )  B_SPLINE_CURVE ( 3, ( #19456, #5524, #17808, #12655 ),
 .UNSPECIFIED., .F., .F. ) 
 B_SPLINE_CURVE_WITH_KNOTS ( ( 4, 4 ),
 ( 1.570796326964226219, 3.141592653589766471 ),
 .UNSPECIFIED. ) 
 CURVE ( )  GEOMETRIC_REPRESENTATION_ITEM ( )  RATIONAL_B_SPLINE_CURVE ( ( 1.000000000000000000, 0.8047378541642826733, 0.8047378541642826733, 1.000000000000000000 ) ) 
 REPRESENTATION_ITEM ( '' )  );
#5668=ADVANCED_FACE ( 'NONE', ( #5873 ), #13010, .T. ) ;
#5696=AXIS2_PLACEMENT_3D ( 'NONE', #18214, #64, #15884 ) ;
#5702=LINE ( 'NONE', #18108, #10271 ) ;
#5730=AXIS2_PLACEMENT_3D ( 'NONE', #18418, #4357, #11496 ) ;
#5738=DIRECTION ( 'NONE',  ( 0.000000000000000000, -1.000000000000000000, 0.000000000000000000 ) ) ;
#5766=DIRECTION ( 'NONE',  ( 0.000000000000000000, -1.000000000000000000, 0.000000000000000000 ) ) ;
#5780=CIRCLE ( 'NONE', #18851, 5.460999999999938126 ) ;
#5873=FACE_OUTER_BOUND ( 'NONE', #20220, .T. ) ;
#5986=ORIENTED_EDGE ( 'NONE', *, *, #9253, .T. ) ;
#6010=ADVANCED_FACE ( 'NONE', ( #4299 ), #6068, .T. ) ;
#6068=CYLINDRICAL_SURFACE ( 'NONE', #13016, 3.175000000000149925 ) ;
#6087=ADVANCED_FACE ( 'NONE', ( #326 ), #20135, .T. ) ;
#6088=EDGE_LOOP ( 'NONE', ( #20831, #21147, #8209, #4866 ) ) ;
#6145=DIRECTION ( 'NONE',  ( 0.000000000000000000, 0.000000000000000000, 1.000000000000000000 ) ) ;
#6153=FACE_OUTER_BOUND ( 'NONE', #11040, .T. ) ;
#6165=CARTESIAN_POINT ( 'NONE',  ( 139.6999999999999886, -3654.043999999999869, 2239.391000000000076 ) ) ;
#6167=AXIS2_PLACEMENT_3D ( 'NONE', #9903, #6411, #20687 ) ;
#6210=FACE_OUTER_BOUND ( 'NONE', #10819, .T. ) ;
#6236=DIRECTION ( 'NONE',  ( 0.000000000000000000, 0.000000000000000000, -1.000000000000000000 ) ) ;
#6253=MANIFOLD_SOLID_BREP ( 'TORNILLO[1]', #6493 ) ;
#6294=EDGE_CURVE ( 'NONE', #4732, #17234, #2849, .T. ) ;
#6299=ADVANCED_FACE ( 'NONE', ( #3231 ), #1740, .T. ) ;
#6411=DIRECTION ( 'NONE',  ( 0.000000000000000000, 0.000000000000000000, -1.000000000000000000 ) ) ;
#6424=CARTESIAN_POINT ( 'NONE',  ( 139.6999999999999886, -3664.965999999999894, 2244.978999999999814 ) ) ;
#6442=CIRCLE ( 'NONE', #5696, 5.080000000000000959 ) ;
#6465=DIRECTION ( 'NONE',  ( -0.8660254037815640071, 0.5000000000049790172, 0.000000000000000000 ) ) ;
#6478=ORIENTED_EDGE ( 'NONE', *, *, #8857, .T. ) ;
#6493=CLOSED_SHELL ( 'NONE', ( #3428, #6010, #14702, #18725, #10489, #5668, #8281, #15263, #18664, #6087, #8655, #18308, #2373, #17877, #18317, #10060, #10520, #12829, #13709, #2959, #19324, #18503, #5270, #12378, #6299, #20042 ) ) ;
#6522=AXIS2_PLACEMENT_3D ( 'NONE', #22355, #16751, #4667 ) ;
#6540=EDGE_CURVE ( 'NONE', #7171, #1044, #12225, .T. ) ;
#6644=( BOUNDED_CURVE ( )  B_SPLINE_CURVE ( 3, ( #1665, #23101, #1900, #19723 ),
 .UNSPECIFIED., .F., .F. ) 
 B_SPLINE_CURVE_WITH_KNOTS ( ( 4, 4 ),
 ( -9.769962616701377556E-15, 1.570796326938358911 ),
 .UNSPECIFIED. ) 
 CURVE ( )  GEOMETRIC_REPRESENTATION_ITEM ( )  RATIONAL_B_SPLINE_CURVE ( ( 1.000000000000000000, 0.8047378540905483213, 0.8047378540905483213, 1.000000000000000000 ) ) 
 REPRESENTATION_ITEM ( '' )  );
#6683=ORIENTED_EDGE ( 'NONE', *, *, #3990, .T. ) ;
#6685=CARTESIAN_POINT ( 'NONE',  ( 139.6999999999986528, -3662.197400000082780, 2239.391000000000076 ) ) ;
#6703=CARTESIAN_POINT ( 'NONE',  ( 134.2390000000000043, -3659.504999999999654, 2239.391000000000076 ) ) ;
#6707=EDGE_CURVE ( 'NONE', #21395, #12304, #15746, .T. ) ;
#6759=( GEOMETRIC_REPRESENTATION_CONTEXT ( 3 ) GLOBAL_UNCERTAINTY_ASSIGNED_CONTEXT ( ( #13217 ) ) GLOBAL_UNIT_ASSIGNED_CONTEXT ( ( #18066, #12789, #16419 ) ) REPRESENTATION_CONTEXT ( 'NONE', 'WORKASPACE' ) );
#6780=DIRECTION ( 'NONE',  ( 6.119339505807659940E-14, -1.000000000000000000, 0.000000000000000000 ) ) ;
#6805=EDGE_CURVE ( 'NONE', #9634, #21213, #13356, .T. ) ;
#6836=FACE_OUTER_BOUND ( 'NONE', #10328, .T. ) ;
#6862=CYLINDRICAL_SURFACE ( 'NONE', #12955, 0.3809999999998149867 ) ;
#6996=VECTOR ( 'NONE', #21384, 1000.000000000000000 ) ;
#7095=CARTESIAN_POINT ( 'NONE',  ( 139.7000000001000046, -3656.812599999999748, 2242.820000000000164 ) ) ;
#7104=DIRECTION ( 'NONE',  ( 1.224646799141920914E-16, -1.000000000000000000, -2.336881798971000421E-14 ) ) ;
#7171=VERTEX_POINT ( 'NONE', #21171 ) ;
#7218=ORIENTED_EDGE ( 'NONE', *, *, #14971, .T. ) ;
#7219=DIRECTION ( 'NONE',  ( 0.000000000000000000, 1.000000000000000000, 0.000000000000000000 ) ) ;
#7232=APPLICATION_CONTEXT ( 'configuration controlled 3d designs of mechanical parts and assemblies' ) ;
#7256=PLANE ( 'NONE',  #7339 ) ;
#7285=DIRECTION ( 'NONE',  ( -2.324635735433000053E-14, 2.336881798971000105E-14, -1.000000000000000000 ) ) ;
#7289=DIRECTION ( 'NONE',  ( -1.000000000000000000, 1.224646799147353207E-16, 0.000000000000000000 ) ) ;
#7301=EDGE_CURVE ( 'NONE', #18199, #20633, #22634, .T. ) ;
#7325=DIRECTION ( 'NONE',  ( -2.903809793931999834E-13, 4.457650181899999573E-12, 1.000000000000000000 ) ) ;
#7339=AXIS2_PLACEMENT_3D ( 'NONE', #106, #12988, #5738 ) ;
#7352=VERTEX_POINT ( 'NONE', #1077 ) ;
#7429=ORIENTED_EDGE ( 'NONE', *, *, #16235, .F. ) ;
#7438=VECTOR ( 'NONE', #12936, 1000.000000000000000 ) ;
#7472=ORIENTED_EDGE ( 'NONE', *, *, #19751, .T. ) ;
#7480=CARTESIAN_POINT ( 'NONE',  ( 139.6999999999999886, -3659.504999999999654, 2270.760000000000218 ) ) ;
#7492=DIRECTION ( 'NONE',  ( -1.000000000000000000, -1.165588477296775430E-12, 0.000000000000000000 ) ) ;
#7520=CARTESIAN_POINT ( 'NONE',  ( 139.6999999997612747, -3662.637340905137989, 2239.009999999999764 ) ) ;
#7545=DIRECTION ( 'NONE',  ( 1.000000000000000000, 0.000000000000000000, 0.000000000000000000 ) ) ;
#7567=LINE ( 'NONE', #21866, #12571 ) ;
#7611=VERTEX_POINT ( 'NONE', #146 ) ;
#7615=EDGE_LOOP ( 'NONE', ( #10672, #7619, #22761, #2585 ) ) ;
#7619=ORIENTED_EDGE ( 'NONE', *, *, #3670, .T. ) ;
#7685=CIRCLE ( 'NONE', #9183, 1.904999999999823501 ) ;
#7689=EDGE_LOOP ( 'NONE', ( #17633, #17679, #8543, #17164 ) ) ;
#7700=TOROIDAL_SURFACE ( 'NONE', #22285, 5.080000000000000071, 0.3810000000000000053 ) ;
#7713=CARTESIAN_POINT ( 'NONE',  ( 139.7000000000001876, -3662.679999999999836, 2245.359999999999673 ) ) ;
#7800=ORIENTED_EDGE ( 'NONE', *, *, #269, .F. ) ;
#7952=CARTESIAN_POINT ( 'NONE',  ( 137.2104978357160405, -3658.067685255075958, 2239.010000000090258 ) ) ;
#7990=CARTESIAN_POINT ( 'NONE',  ( 134.2390000000000043, -3659.504999999999654, 2244.978999999999814 ) ) ;
#8000=( BOUNDED_CURVE ( )  B_SPLINE_CURVE ( 3, ( #22943, #10182, #17327, #8441 ),
 .UNSPECIFIED., .F., .T. ) 
 B_SPLINE_CURVE_WITH_KNOTS ( ( 4, 4 ),
 ( 1.570796327224941002, 3.141592653589829531 ),
 .UNSPECIFIED. ) 
 CURVE ( )  GEOMETRIC_REPRESENTATION_ITEM ( )  RATIONAL_B_SPLINE_CURVE ( ( 1.000000000000000000, 0.8047378542257188627, 0.8047378542257188627, 1.000000000000000000 ) ) 
 REPRESENTATION_ITEM ( '' )  );
#8020=TOROIDAL_SURFACE ( 'NONE', #12502, 5.080000000000000071, 0.3810000000000000053 ) ;
#8047=EDGE_LOOP ( 'NONE', ( #506, #5063, #2283, #5490, #2234 ) ) ;
#8077=DIRECTION ( 'NONE',  ( -0.8660254037840939834, -0.5000000000005969669, 0.000000000000000000 ) ) ;
#8112=VERTEX_POINT ( 'NONE', #7095 ) ;
#8167=EDGE_LOOP ( 'NONE', ( #3089, #22710, #38, #685 ) ) ;
#8175=CARTESIAN_POINT ( 'NONE',  ( 142.0316867971999955, -3660.851200000000063, 2242.820000000000164 ) ) ;
#8209=ORIENTED_EDGE ( 'NONE', *, *, #12730, .F. ) ;
#8213=EDGE_CURVE ( 'NONE', #2120, #565, #5780, .T. ) ;
#8226=EDGE_CURVE ( 'NONE', #13348, #21213, #17869, .T. ) ;
#8228=CARTESIAN_POINT ( 'NONE',  ( 136.9873132028999976, -3661.071170452999922, 2239.009999999999764 ) ) ;
#8240=CARTESIAN_POINT ( 'NONE',  ( 139.6999999999999886, -3659.504999999999654, 2244.978999999999814 ) ) ;
#8281=ADVANCED_FACE ( 'NONE', ( #14359 ), #12600, .F. ) ;
#8338=CIRCLE ( 'NONE', #5730, 5.460999999999938126 ) ;
#8347=ORIENTED_EDGE ( 'NONE', *, *, #8226, .T. ) ;
#8360=EDGE_CURVE ( 'NONE', #21395, #11858, #16788, .T. ) ;
#8385=ORIENTED_EDGE ( 'NONE', *, *, #11518, .F. ) ;
#8441=CARTESIAN_POINT ( 'NONE',  ( 139.7000000000063835, -3656.812599999938357, 2239.391000000000076 ) ) ;
#8446=AXIS2_PLACEMENT_3D ( 'NONE', #7480, #229, #19794 ) ;
#8482=DIRECTION ( 'NONE',  ( 2.324635735433000053E-14, 0.000000000000000000, 1.000000000000000000 ) ) ;
#8500=TOROIDAL_SURFACE ( 'NONE', #16720, 1.905000000000000027, 1.270000000000000018 ) ;
#8502=CARTESIAN_POINT ( 'NONE',  ( 139.6999999999999886, -3657.599999999999909, 2270.760000000000218 ) ) ;
#8539=VERTEX_POINT ( 'NONE', #5193 ) ;
#8543=ORIENTED_EDGE ( 'NONE', *, *, #13450, .F. ) ;
#8655=ADVANCED_FACE ( 'NONE', ( #12449 ), #19597, .T. ) ;
#8712=EDGE_CURVE ( 'NONE', #19931, #3802, #3334, .T. ) ;
#8715=DIRECTION ( 'NONE',  ( 0.000000000000000000, 0.000000000000000000, -1.000000000000000000 ) ) ;
#8716=AXIS2_PLACEMENT_3D ( 'NONE', #3942, #11864, #12849 ) ;
#8732=DIRECTION ( 'NONE',  ( -0.5000000000043488546, -0.8660254037819278272, 0.000000000000000000 ) ) ;
#8739=VECTOR ( 'NONE', #9157, 999.9999999999998863 ) ;
#8788=ORIENTED_EDGE ( 'NONE', *, *, #8712, .F. ) ;
#8857=EDGE_CURVE ( 'NONE', #15808, #9634, #20179, .T. ) ;
#8959=AXIS2_PLACEMENT_3D ( 'NONE', #1821, #17393, #13899 ) ;
#9039=ORIENTED_EDGE ( 'NONE', *, *, #6805, .T. ) ;
#9157=DIRECTION ( 'NONE',  ( 0.8660254037817188832, -0.5000000000047110094, -1.484475890921031808E-12 ) ) ;
#9183=AXIS2_PLACEMENT_3D ( 'NONE', #22053, #14811, #20637 ) ;
#9228=PRODUCT_CONTEXT ( 'NONE', #11555, 'mechanical' ) ;
#9253=EDGE_CURVE ( 'NONE', #21213, #9634, #18620, .T. ) ;
#9278=LINE ( 'NONE', #2006, #8739 ) ;
#9334=DIRECTION ( 'NONE',  ( 0.8660254037825932949, 0.5000000000031962211, 0.000000000000000000 ) ) ;
#9374=DIRECTION ( 'NONE',  ( 1.206643234470999950E-12, -1.000000000000000000, -2.336881798973999985E-14 ) ) ;
#9417=VERTEX_POINT ( 'NONE', #9871 ) ;
#9443=EDGE_LOOP ( 'NONE', ( #19034, #22186 ) ) ;
#9445=DIRECTION ( 'NONE',  ( 0.5000000000031885605, -0.8660254037825977358, 0.000000000000000000 ) ) ;
#9463=PLANE ( 'NONE',  #17729 ) ;
#9467=CIRCLE ( 'NONE', #836, 1.269999999999882334 ) ;
#9485=CARTESIAN_POINT ( 'NONE',  ( 142.4126867972000241, -3659.504999999999654, 2239.391000000000076 ) ) ;
#9634=VERTEX_POINT ( 'NONE', #21253 ) ;
#9662=CARTESIAN_POINT ( 'NONE',  ( 139.6999999999999886, -3664.965999999999894, 2245.359999999999673 ) ) ;
#9685=DIRECTION ( 'NONE',  ( 0.000000000000000000, 0.000000000000000000, -1.000000000000000000 ) ) ;
#9708=EDGE_CURVE ( 'NONE', #19068, #21395, #10925, .T. ) ;
#9751=DIRECTION ( 'NONE',  ( 0.000000000000000000, 0.000000000000000000, 1.000000000000000000 ) ) ;
#9812=ORIENTED_EDGE ( 'NONE', *, *, #6707, .F. ) ;
#9871=CARTESIAN_POINT ( 'NONE',  ( 137.3683132029982517, -3658.158799999858729, 2239.391000000000076 ) ) ;
#9903=CARTESIAN_POINT ( 'NONE',  ( 139.6999999999999886, -3659.504999999999654, 2245.359999999999673 ) ) ;
#9978=CARTESIAN_POINT ( 'NONE',  ( 144.7800000000000011, -3659.504999999999654, 2239.009999999999764 ) ) ;
#10060=ADVANCED_FACE ( 'NONE', ( #19573 ), #2116, .T. ) ;
#10068=CARTESIAN_POINT ( 'NONE',  ( 139.6999999999999886, -3659.504999999999654, 2239.391000000000076 ) ) ;
#10151=ORIENTED_EDGE ( 'NONE', *, *, #3051, .T. ) ;
#10175=VECTOR ( 'NONE', #13829, 1000.000000000000000 ) ;
#10182=CARTESIAN_POINT ( 'NONE',  ( 139.7000000000068383, -3656.630370510378725, 2239.010000000095715 ) ) ;
#10204=CARTESIAN_POINT ( 'NONE',  ( 142.0316867971391446, -3658.158799999964231, 2239.391000000000076 ) ) ;
#10243=CARTESIAN_POINT ( 'NONE',  ( 139.6999999999999886, -3659.504999999999654, 2239.391000000000076 ) ) ;
#10248=ORIENTED_EDGE ( 'NONE', *, *, #15852, .T. ) ;
#10271=VECTOR ( 'NONE', #12724, 1000.000000000000000 ) ;
#10307=LINE ( 'NONE', #15818, #3224 ) ;
#10328=EDGE_LOOP ( 'NONE', ( #20417, #1792, #18331, #11539, #3494 ) ) ;
#10432=FACE_BOUND ( 'NONE', #10445, .T. ) ;
#10445=EDGE_LOOP ( 'NONE', ( #5986, #9039 ) ) ;
#10448=DIRECTION ( 'NONE',  ( 0.000000000000000000, -1.000000000000000000, 0.000000000000000000 ) ) ;
#10466=ORIENTED_EDGE ( 'NONE', *, *, #15117, .T. ) ;
#10468=ORIENTED_EDGE ( 'NONE', *, *, #47, .T. ) ;
#10477=DIRECTION ( 'NONE',  ( 0.8660254037820785955, -0.5000000000040877302, -3.181634500919918361E-14 ) ) ;
#10489=ADVANCED_FACE ( 'NONE', ( #12120 ), #7700, .T. ) ;
#10499=DIRECTION ( 'NONE',  ( 0.000000000000000000, 1.000000000000000000, 0.000000000000000000 ) ) ;
#10520=ADVANCED_FACE ( 'NONE', ( #5218 ), #6862, .T. ) ;
#10628=CARTESIAN_POINT ( 'NONE',  ( 139.6999999999999886, -3657.599999999999909, 2272.030000000000200 ) ) ;
#10635=DIRECTION ( 'NONE',  ( 0.5000000000047859494, 0.8660254037816754735, 0.000000000000000000 ) ) ;
#10655=AXIS2_PLACEMENT_3D ( 'NONE', #16211, #21612, #17966 ) ;
#10672=ORIENTED_EDGE ( 'NONE', *, *, #341, .T. ) ;
#10690=EDGE_CURVE ( 'NONE', #2348, #9417, #3791, .T. ) ;
#10691=CARTESIAN_POINT ( 'NONE',  ( 139.6999999999999886, -3659.504999999999654, 2239.391000000000076 ) ) ;
#10707=ORIENTED_EDGE ( 'NONE', *, *, #13866, .F. ) ;
#10819=EDGE_LOOP ( 'NONE', ( #10468, #10466, #18973, #5206 ) ) ;
#10835=CARTESIAN_POINT ( 'NONE',  ( 139.6999999999999886, -3662.679999999999836, 2270.760000000000218 ) ) ;
#10898=DIRECTION ( 'NONE',  ( 0.000000000000000000, 0.000000000000000000, -1.000000000000000000 ) ) ;
#10925=LINE ( 'NONE', #12570, #2140 ) ;
#10969=DIRECTION ( 'NONE',  ( -0.8660254037820102058, 0.5000000000042060799, 1.814359422182020449E-12 ) ) ;
#11035=CARTESIAN_POINT ( 'NONE',  ( 139.6999999999985675, -3662.379629489635590, 2239.010000000083437 ) ) ;
#11040=EDGE_LOOP ( 'NONE', ( #7429, #15139, #16606, #11322, #14364, #7800 ) ) ;
#11056=ORIENTED_EDGE ( 'NONE', *, *, #5435, .T. ) ;
#11125=VERTEX_POINT ( 'NONE', #13934 ) ;
#11135=AXIS2_PLACEMENT_3D ( 'NONE', #2141, #21817, #5550 ) ;
#11182=CARTESIAN_POINT ( 'NONE',  ( 139.6999999999999886, -3659.504999999999654, 2244.978999999999814 ) ) ;
#11184=CARTESIAN_POINT ( 'NONE',  ( 139.6999999999999886, -3659.504999999999654, 2270.760000000000218 ) ) ;
#11198=CARTESIAN_POINT ( 'NONE',  ( 141.0563433985999779, -3661.854255679000289, 2239.391000000000076 ) ) ;
#11322=ORIENTED_EDGE ( 'NONE', *, *, #19292, .T. ) ;
#11329=VECTOR ( 'NONE', #12901, 1000.000000000000114 ) ;
#11381=EDGE_CURVE ( 'NONE', #7352, #19931, #13094, .T. ) ;
#11388=CIRCLE ( 'NONE', #21885, 5.080000000000000959 ) ;
#11399=CARTESIAN_POINT ( 'NONE',  ( 142.0316867971999955, -3660.851200000000063, 2242.820000000000164 ) ) ;
#11410=DIRECTION ( 'NONE',  ( 0.000000000000000000, 0.000000000000000000, -1.000000000000000000 ) ) ;
#11468=CARTESIAN_POINT ( 'NONE',  ( 138.3436566013999993, -3657.155744320999929, 2239.391000000000076 ) ) ;
#11496=DIRECTION ( 'NONE',  ( 0.000000000000000000, -1.000000000000000000, 0.000000000000000000 ) ) ;
#11518=EDGE_CURVE ( 'NONE', #2348, #5217, #5702, .T. ) ;
#11526=DIRECTION ( 'NONE',  ( 0.000000000000000000, -1.000000000000000000, 0.000000000000000000 ) ) ;
#11539=ORIENTED_EDGE ( 'NONE', *, *, #8213, .T. ) ;
#11549=CYLINDRICAL_SURFACE ( 'NONE', #6167, 5.460999999999938126 ) ;
#11555=APPLICATION_CONTEXT ( 'configuration controlled 3d designs of mechanical parts and assemblies' ) ;
#11669=EDGE_CURVE ( 'NONE', #8539, #1092, #11388, .T. ) ;
#11679=ORIENTED_EDGE ( 'NONE', *, *, #269, .T. ) ;
#11691=CYLINDRICAL_SURFACE ( 'NONE', #524, 0.3809999999999180154 ) ;
#11788=AXIS2_PLACEMENT_3D ( 'NONE', #20724, #15341, #22474 ) ;
#11816=FACE_OUTER_BOUND ( 'NONE', #22599, .T. ) ;
#11858=VERTEX_POINT ( 'NONE', #2005 ) ;
#11864=DIRECTION ( 'NONE',  ( -0.5000000000047110094, -0.8660254037817188832, 0.000000000000000000 ) ) ;
#11883=AXIS2_PLACEMENT_3D ( 'NONE', #18358, #18247, #14629 ) ;
#12040=VECTOR ( 'NONE', #15375, 1000.000000000000000 ) ;
#12056=EDGE_LOOP ( 'NONE', ( #21294, #7472, #13803, #22740, #5292, #2951 ) ) ;
#12067=ORIENTED_EDGE ( 'NONE', *, *, #20113, .F. ) ;
#12120=FACE_OUTER_BOUND ( 'NONE', #15999, .T. ) ;
#12143=CARTESIAN_POINT ( 'NONE',  ( 142.0316867971391446, -3658.158799999964231, 2239.391000000000076 ) ) ;
#12167=VECTOR ( 'NONE', #11410, 1000.000000000000000 ) ;
#12196=CARTESIAN_POINT ( 'NONE',  ( 139.7000000002931301, -3656.372659094888149, 2239.009999999999764 ) ) ;
#12215=DIRECTION ( 'NONE',  ( 1.000000000000000000, 5.432398939370942693E-28, -2.324635735433000053E-14 ) ) ;
#12225=CIRCLE ( 'NONE', #21585, 5.460999999999938126 ) ;
#12228=ORIENTED_EDGE ( 'NONE', *, *, #11669, .T. ) ;
#12257=VECTOR ( 'NONE', #6236, 1000.000000000000000 ) ;
#12279=CIRCLE ( 'NONE', #14526, 0.3809999999999647002 ) ;
#12304=VERTEX_POINT ( 'NONE', #12873 ) ;
#12335=LINE ( 'NONE', #17842, #16910 ) ;
#12357=DIRECTION ( 'NONE',  ( -2.324635735433000053E-14, 2.336881798971000105E-14, -1.000000000000000000 ) ) ;
#12378=ADVANCED_FACE ( 'NONE', ( #14405 ), #2103, .T. ) ;
#12418=ORIENTED_EDGE ( 'NONE', *, *, #16235, .T. ) ;
#12449=FACE_OUTER_BOUND ( 'NONE', #18584, .T. ) ;
#12502=AXIS2_PLACEMENT_3D ( 'NONE', #15691, #17434, #1613 ) ;
#12514=( BOUNDED_CURVE ( )  B_SPLINE_CURVE ( 3, ( #5126, #19526, #19412, #12143 ),
 .UNSPECIFIED., .F., .F. ) 
 B_SPLINE_CURVE_WITH_KNOTS ( ( 4, 4 ),
 ( 1.570796326272141830, 3.141592653589783346 ),
 .UNSPECIFIED. ) 
 CURVE ( )  GEOMETRIC_REPRESENTATION_ITEM ( )  RATIONAL_B_SPLINE_CURVE ( ( 1.000000000000000000, 0.8047378540011528303, 0.8047378540011528303, 1.000000000000000000 ) ) 
 REPRESENTATION_ITEM ( '' )  );
#12552=CARTESIAN_POINT ( 'NONE',  ( 137.3683132029000262, -3658.158799999999701, 2239.391000000000076 ) ) ;
#12560=CARTESIAN_POINT ( 'NONE',  ( 139.6999999999999886, -3661.409999999999400, 2270.760000000000218 ) ) ;
#12570=CARTESIAN_POINT ( 'NONE',  ( 142.0316867971999955, -3660.851200000000063, 2239.391000000000076 ) ) ;
#12571=VECTOR ( 'NONE', #12963, 1000.000000000000000 ) ;
#12600=PLANE ( 'NONE',  #18222 ) ;
#12610=CARTESIAN_POINT ( 'NONE',  ( 139.6999999999999886, -3659.504999999999654, 2270.760000000000218 ) ) ;
#12655=CARTESIAN_POINT ( 'NONE',  ( 142.0316867971266390, -3660.851200000091012, 2239.391000000000076 ) ) ;
#12701=CARTESIAN_POINT ( 'NONE',  ( 139.6999999999999886, -3662.679999999999836, 2270.760000000000218 ) ) ;
#12706=ORIENTED_EDGE ( 'NONE', *, *, #18877, .F. ) ;
#12724=DIRECTION ( 'NONE',  ( 7.422379454677999805E-13, -1.000000000000000000, 4.288485907146999317E-12 ) ) ;
#12730=EDGE_CURVE ( 'NONE', #11858, #5217, #17407, .T. ) ;
#12784=DIRECTION ( 'NONE',  ( -1.000000000000000000, 0.000000000000000000, 2.324635735433000053E-14 ) ) ;
#12789=( NAMED_UNIT ( * ) PLANE_ANGLE_UNIT ( ) SI_UNIT ( $, .RADIAN. ) );
#12810=ORIENTED_EDGE ( 'NONE', *, *, #13274, .F. ) ;
#12829=ADVANCED_FACE ( 'NONE', ( #14499 ), #17887, .T. ) ;
#12845=TOROIDAL_SURFACE ( 'NONE', #22524, 5.080000000000000071, 0.3810000000000000053 ) ;
#12849=DIRECTION ( 'NONE',  ( -0.8660254037817187722, 0.5000000000047108983, 0.000000000000000000 ) ) ;
#12873=CARTESIAN_POINT ( 'NONE',  ( 142.0316867971999955, -3658.158799999999701, 2242.820000000000164 ) ) ;
#12901=DIRECTION ( 'NONE',  ( 0.8660254037827048723, 0.5000000000030029312, 0.000000000000000000 ) ) ;
#12907=VECTOR ( 'NONE', #18316, 1000.000000000000000 ) ;
#12936=DIRECTION ( 'NONE',  ( 0.000000000000000000, 0.000000000000000000, -1.000000000000000000 ) ) ;
#12955=AXIS2_PLACEMENT_3D ( 'NONE', #14006, #10477, #8732 ) ;
#12963=DIRECTION ( 'NONE',  ( 0.8660254037821217832, -0.5000000000040129011, 0.000000000000000000 ) ) ;
#12988=DIRECTION ( 'NONE',  ( 0.000000000000000000, 0.000000000000000000, -1.000000000000000000 ) ) ;
#13010=CYLINDRICAL_SURFACE ( 'NONE', #19350, 0.3809999999999924558 ) ;
#13016=AXIS2_PLACEMENT_3D ( 'NONE', #14861, #9685, #2315 ) ;
#13035=CIRCLE ( 'NONE', #2917, 0.3809999999999647002 ) ;
#13094=LINE ( 'NONE', #15086, #14768 ) ;
#13177=ORIENTED_EDGE ( 'NONE', *, *, #10690, .F. ) ;
#13217=UNCERTAINTY_MEASURE_WITH_UNIT (LENGTH_MEASURE( 1.000000000000000082E-05 ), #18066, 'distance_accuracy_value', 'NONE');
#13237=CARTESIAN_POINT ( 'NONE',  ( 139.6999999999999886, -3654.043999999999869, 2244.978999999999814 ) ) ;
#13265=CARTESIAN_POINT ( 'NONE',  ( 139.6999999999999886, -3664.965999999999894, 2239.391000000000076 ) ) ;
#13274=EDGE_CURVE ( 'NONE', #12304, #19181, #21724, .T. ) ;
#13286=CYLINDRICAL_SURFACE ( 'NONE', #14045, 5.460999999999938126 ) ;
#13307=SHAPE_DEFINITION_REPRESENTATION ( #1714, #5332 ) ;
#13338=CARTESIAN_POINT ( 'NONE',  ( 136.9873132030510305, -3657.938829547328169, 2239.009999999999764 ) ) ;
#13348=VERTEX_POINT ( 'NONE', #12701 ) ;
#13356=CIRCLE ( 'NONE', #14494, 3.175000000000149925 ) ;
#13358=ORIENTED_EDGE ( 'NONE', *, *, #6707, .T. ) ;
#13368=CARTESIAN_POINT ( 'NONE',  ( 139.6999999999999886, -3656.329999999999472, 2270.760000000000218 ) ) ;
#13404=ORIENTED_EDGE ( 'NONE', *, *, #20802, .F. ) ;
#13450=EDGE_CURVE ( 'NONE', #15441, #21028, #7685, .T. ) ;
#13507=DIRECTION ( 'NONE',  ( 0.000000000000000000, -1.000000000000000000, 0.000000000000000000 ) ) ;
#13510=DIRECTION ( 'NONE',  ( -1.000000000000000000, 0.000000000000000000, 2.324635735433000053E-14 ) ) ;
#13511=EDGE_CURVE ( 'NONE', #1438, #17234, #15166, .T. ) ;
#13513=VERTEX_POINT ( 'NONE', #5065 ) ;
#13528=ORIENTED_EDGE ( 'NONE', *, *, #13274, .T. ) ;
#13532=( BOUNDED_CURVE ( )  B_SPLINE_CURVE ( 3, ( #16843, #20366, #7952, #13338 ),
 .UNSPECIFIED., .F., .T. ) 
 B_SPLINE_CURVE_WITH_KNOTS ( ( 4, 4 ),
 ( -2.664535259100375697E-14, 1.570796326393333997 ),
 .UNSPECIFIED. ) 
 CURVE ( )  GEOMETRIC_REPRESENTATION_ITEM ( )  RATIONAL_B_SPLINE_CURVE ( ( 1.000000000000000000, 0.8047378542190078976, 0.8047378542190078976, 1.000000000000000000 ) ) 
 REPRESENTATION_ITEM ( '' )  );
#13709=ADVANCED_FACE ( 'NONE', ( #19472, #14324 ), #14441, .T. ) ;
#13725=CARTESIAN_POINT ( 'NONE',  ( 142.0316867971999955, -3658.158799999999701, 2239.391000000000076 ) ) ;
#13803=ORIENTED_EDGE ( 'NONE', *, *, #7301, .T. ) ;
#13827=ORIENTED_EDGE ( 'NONE', *, *, #4223, .F. ) ;
#13829=DIRECTION ( 'NONE',  ( -2.824627736850999825E-12, 1.000000000000000000, 0.000000000000000000 ) ) ;
#13866=EDGE_CURVE ( 'NONE', #3802, #13513, #18402, .T. ) ;
#13899=DIRECTION ( 'NONE',  ( 0.000000000000000000, 1.000000000000000000, 0.000000000000000000 ) ) ;
#13929=DIRECTION ( 'NONE',  ( -0.8660254037817188832, 0.5000000000047110094, 3.181634500920069822E-14 ) ) ;
#13934=CARTESIAN_POINT ( 'NONE',  ( 136.9873132028999976, -3661.071170452878050, 2239.009999999999764 ) ) ;
#14006=CARTESIAN_POINT ( 'NONE',  ( 138.3436566013999993, -3661.854255679000289, 2239.391000000000076 ) ) ;
#14025=DIRECTION ( 'NONE',  ( 0.8660254037826368156, 0.5000000000031208369, 0.000000000000000000 ) ) ;
#14036=ORIENTED_EDGE ( 'NONE', *, *, #3640, .T. ) ;
#14037=ORIENTED_EDGE ( 'NONE', *, *, #19751, .F. ) ;
#14038=PLANE ( 'NONE',  #17293 ) ;
#14045=AXIS2_PLACEMENT_3D ( 'NONE', #20437, #4387, #11526 ) ;
#14063=DIRECTION ( 'NONE',  ( 1.000000000000000000, 5.432398939370942693E-28, -2.324635735433000053E-14 ) ) ;
#14073=CARTESIAN_POINT ( 'NONE',  ( 134.6199999999999761, -3659.504999999999654, 2239.391000000000076 ) ) ;
#14110=VERTEX_POINT ( 'NONE', #6165 ) ;
#14133=CARTESIAN_POINT ( 'NONE',  ( 139.6999999999999886, -3656.329999999999472, 2270.760000000000218 ) ) ;
#14143=AXIS2_PLACEMENT_3D ( 'NONE', #10691, #21479, #3656 ) ;
#14189=CARTESIAN_POINT ( 'NONE',  ( 139.6999999999999886, -3659.504999999999654, 2245.359999999999673 ) ) ;
#14305=EDGE_CURVE ( 'NONE', #15808, #15441, #15084, .T. ) ;
#14324=FACE_OUTER_BOUND ( 'NONE', #2949, .T. ) ;
#14359=FACE_OUTER_BOUND ( 'NONE', #15768, .T. ) ;
#14364=ORIENTED_EDGE ( 'NONE', *, *, #6540, .F. ) ;
#14405=FACE_OUTER_BOUND ( 'NONE', #4444, .T. ) ;
#14441=PLANE ( 'NONE',  #2811 ) ;
#14478=DIRECTION ( 'NONE',  ( 0.000000000000000000, -1.000000000000000000, 4.457650181899999573E-12 ) ) ;
#14494=AXIS2_PLACEMENT_3D ( 'NONE', #19262, #8715, #15861 ) ;
#14499=FACE_OUTER_BOUND ( 'NONE', #16228, .T. ) ;
#14523=FACE_OUTER_BOUND ( 'NONE', #9443, .T. ) ;
#14526=AXIS2_PLACEMENT_3D ( 'NONE', #4382, #16906, #18669 ) ;
#14579=ORIENTED_EDGE ( 'NONE', *, *, #5435, .F. ) ;
#14629=DIRECTION ( 'NONE',  ( 0.000000000000000000, 0.000000000000000000, -1.000000000000000000 ) ) ;
#14702=ADVANCED_FACE ( 'NONE', ( #6836 ), #12845, .T. ) ;
#14768=VECTOR ( 'NONE', #2652, 1000.000000000000114 ) ;
#14778=ORIENTED_EDGE ( 'NONE', *, *, #3509, .T. ) ;
#14811=DIRECTION ( 'NONE',  ( 0.000000000000000000, 0.000000000000000000, 1.000000000000000000 ) ) ;
#14861=CARTESIAN_POINT ( 'NONE',  ( 139.6999999999999886, -3659.504999999999654, 2270.760000000000218 ) ) ;
#14903=EDGE_LOOP ( 'NONE', ( #20609, #12810, #19615, #4592 ) ) ;
#14971=EDGE_CURVE ( 'NONE', #4732, #20464, #18044, .T. ) ;
#14993=DIRECTION ( 'NONE',  ( 1.000000000000000000, 2.331176954593550859E-12, 0.000000000000000000 ) ) ;
#15084=CIRCLE ( 'NONE', #4603, 1.269999999999882334 ) ;
#15086=CARTESIAN_POINT ( 'NONE',  ( 137.3683132029000262, -3660.851200000000063, 2239.391000000000076 ) ) ;
#15117=EDGE_CURVE ( 'NONE', #9417, #20633, #13532, .T. ) ;
#15139=ORIENTED_EDGE ( 'NONE', *, *, #16082, .F. ) ;
#15166=CIRCLE ( 'NONE', #3570, 5.460999999999938126 ) ;
#15194=VECTOR ( 'NONE', #4642, 1000.000000000000114 ) ;
#15225=DIRECTION ( 'NONE',  ( -0.5000000000007168710, 0.8660254037840248165, 0.000000000000000000 ) ) ;
#15242=ORIENTED_EDGE ( 'NONE', *, *, #17018, .T. ) ;
#15263=ADVANCED_FACE ( 'NONE', ( #21306 ), #14038, .T. ) ;
#15288=ORIENTED_EDGE ( 'NONE', *, *, #9253, .F. ) ;
#15341=DIRECTION ( 'NONE',  ( 5.432398939370942693E-28, 1.000000000000000000, 2.336881798971000105E-14 ) ) ;
#15368=EDGE_LOOP ( 'NONE', ( #1269, #788, #17610, #16315 ) ) ;
#15375=DIRECTION ( 'NONE',  ( -1.169647906252999915E-12, 1.000000000000000000, 0.000000000000000000 ) ) ;
#15410=ORIENTED_EDGE ( 'NONE', *, *, #5302, .T. ) ;
#15418=CIRCLE ( 'NONE', #5319, 5.460999999999938126 ) ;
#15441=VERTEX_POINT ( 'NONE', #10628 ) ;
#15452=CYLINDRICAL_SURFACE ( 'NONE', #3496, 0.3809999999999260090 ) ;
#15591=DIRECTION ( 'NONE',  ( 2.347365683444999541E-13, 0.000000000000000000, -1.000000000000000000 ) ) ;
#15679=DIRECTION ( 'NONE',  ( 0.000000000000000000, 0.000000000000000000, -1.000000000000000000 ) ) ;
#15691=CARTESIAN_POINT ( 'NONE',  ( 139.6999999999999886, -3659.504999999999654, 2244.978999999999814 ) ) ;
#15730=ORIENTED_EDGE ( 'NONE', *, *, #20301, .T. ) ;
#15746=LINE ( 'NONE', #1556, #18211 ) ;
#15757=DIRECTION ( 'NONE',  ( -1.052267375338999979E-13, 2.590196616219000170E-13, -1.000000000000000000 ) ) ;
#15768=EDGE_LOOP ( 'NONE', ( #23011, #22241, #8385, #18456, #19959, #9812 ) ) ;
#15808=VERTEX_POINT ( 'NONE', #14133 ) ;
#15812=LINE ( 'NONE', #22598, #10175 ) ;
#15818=CARTESIAN_POINT ( 'NONE',  ( 137.3683132029000262, -3660.851200000000063, 2242.820000000000164 ) ) ;
#15852=EDGE_CURVE ( 'NONE', #20464, #4732, #6442, .T. ) ;
#15858=VECTOR ( 'NONE', #364, 1000.000000000000000 ) ;
#15861=DIRECTION ( 'NONE',  ( 6.119339505807659940E-14, -1.000000000000000000, 0.000000000000000000 ) ) ;
#15866=EDGE_CURVE ( 'NONE', #15808, #13348, #19910, .T. ) ;
#15884=DIRECTION ( 'NONE',  ( -1.000000000000000000, 0.000000000000000000, 0.000000000000000000 ) ) ;
#15999=EDGE_LOOP ( 'NONE', ( #20378, #14036, #11056, #16412, #1087 ) ) ;
#16018=AXIS2_PLACEMENT_3D ( 'NONE', #3016, #15679, #6780 ) ;
#16057=DIRECTION ( 'NONE',  ( 1.224646799141920914E-16, -1.000000000000000000, -2.336881798971000421E-14 ) ) ;
#16082=EDGE_CURVE ( 'NONE', #565, #1438, #15418, .T. ) ;
#16105=CARTESIAN_POINT ( 'NONE',  ( 142.4126867973298545, -3657.938829547075329, 2239.009999999999764 ) ) ;
#16119=PRODUCT_DEFINITION_FORMATION_WITH_SPECIFIED_SOURCE ( 'ANY', '', #5080, .NOT_KNOWN. ) ;
#16203=VECTOR ( 'NONE', #22290, 1000.000000000000000 ) ;
#16211=CARTESIAN_POINT ( 'NONE',  ( 139.6999999999999886, -3659.504999999999654, 2244.978999999999814 ) ) ;
#16228=EDGE_LOOP ( 'NONE', ( #15730, #13827, #10707, #8788 ) ) ;
#16234=DIRECTION ( 'NONE',  ( 0.000000000000000000, 0.000000000000000000, 1.000000000000000000 ) ) ;
#16235=EDGE_CURVE ( 'NONE', #1438, #14110, #12335, .T. ) ;
#16238=DIRECTION ( 'NONE',  ( 1.000000000000000000, 0.000000000000000000, 0.000000000000000000 ) ) ;
#16315=ORIENTED_EDGE ( 'NONE', *, *, #5008, .F. ) ;
#16318=VECTOR ( 'NONE', #14025, 1000.000000000000114 ) ;
#16336=CARTESIAN_POINT ( 'NONE',  ( 142.0316867971999955, -3658.158799999999701, 2242.820000000000164 ) ) ;
#16401=CARTESIAN_POINT ( 'NONE',  ( 136.9873132028999976, -3659.504999999999654, 2239.391000000000076 ) ) ;
#16411=DIRECTION ( 'NONE',  ( -2.324635735433000053E-14, 0.000000000000000000, -1.000000000000000000 ) ) ;
#16412=ORIENTED_EDGE ( 'NONE', *, *, #3509, .F. ) ;
#16419=( NAMED_UNIT ( * ) SI_UNIT ( $, .STERADIAN. ) SOLID_ANGLE_UNIT ( ) );
#16605=CARTESIAN_POINT ( 'NONE',  ( 139.6999999999999886, -3662.197400000000016, 2242.820000000000164 ) ) ;
#16606=ORIENTED_EDGE ( 'NONE', *, *, #8213, .F. ) ;
#16664=DIRECTION ( 'NONE',  ( -0.8660254037842058938, -0.5000000000004030110, 0.000000000000000000 ) ) ;
#16707=EDGE_LOOP ( 'NONE', ( #4117, #12418, #2165, #17150, #18957, #13404 ) ) ;
#16720=AXIS2_PLACEMENT_3D ( 'NONE', #5122, #19409, #10499 ) ;
#16726=ORIENTED_EDGE ( 'NONE', *, *, #8226, .F. ) ;
#16741=UNCERTAINTY_MEASURE_WITH_UNIT (LENGTH_MEASURE( 1.000000000000000082E-05 ), #21126, 'distance_accuracy_value', 'NONE');
#16751=DIRECTION ( 'NONE',  ( 0.5000000000005969669, -0.8660254037840939834, 0.000000000000000000 ) ) ;
#16788=LINE ( 'NONE', #11399, #4373 ) ;
#16790=DIRECTION ( 'NONE',  ( 0.000000000000000000, 1.000000000000000000, 0.000000000000000000 ) ) ;
#16843=CARTESIAN_POINT ( 'NONE',  ( 137.3683132029982517, -3658.158799999858729, 2239.391000000000076 ) ) ;
#16859=CARTESIAN_POINT ( 'NONE',  ( 142.4126867972000241, -3657.938829547000296, 2239.009999999999764 ) ) ;
#16892=LINE ( 'NONE', #8228, #12040 ) ;
#16906=DIRECTION ( 'NONE',  ( 5.432398939370942693E-28, 1.000000000000000000, 2.336881798971000105E-14 ) ) ;
#16910=VECTOR ( 'NONE', #19485, 1000.000000000000000 ) ;
#17002=AXIS2_PLACEMENT_3D ( 'NONE', #17758, #3344, #20816 ) ;
#17018=EDGE_CURVE ( 'NONE', #22138, #13513, #20538, .T. ) ;
#17059=LINE ( 'NONE', #2766, #15194 ) ;
#17089=DIRECTION ( 'NONE',  ( -0.8660254037816071948, 0.5000000000049040771, 0.000000000000000000 ) ) ;
#17126=AXIS2_PLACEMENT_3D ( 'NONE', #4607, #22522, #13510 ) ;
#17150=ORIENTED_EDGE ( 'NONE', *, *, #3640, .F. ) ;
#17164=ORIENTED_EDGE ( 'NONE', *, *, #14305, .F. ) ;
#17168=EDGE_LOOP ( 'NONE', ( #21713, #1678, #12067, #3169 ) ) ;
#17234=VERTEX_POINT ( 'NONE', #7990 ) ;
#17250=VECTOR ( 'NONE', #15757, 1000.000000000000000 ) ;
#17293=AXIS2_PLACEMENT_3D ( 'NONE', #22696, #21189, #17416 ) ;
#17307=EDGE_CURVE ( 'NONE', #18165, #14110, #8338, .T. ) ;
#17327=CARTESIAN_POINT ( 'NONE',  ( 139.7000000000063835, -3656.812599999822851, 2239.167815367340609 ) ) ;
#17348=DIRECTION ( 'NONE',  ( 2.324635735433000053E-14, 0.000000000000000000, 1.000000000000000000 ) ) ;
#17393=DIRECTION ( 'NONE',  ( 0.000000000000000000, 0.000000000000000000, 1.000000000000000000 ) ) ;
#17407=LINE ( 'NONE', #4052, #546 ) ;
#17416=DIRECTION ( 'NONE',  ( -2.848935406719999894E-12, 1.000000000000000000, 0.000000000000000000 ) ) ;
#17434=DIRECTION ( 'NONE',  ( -2.324635735433000053E-14, 2.336881798971000105E-14, -1.000000000000000000 ) ) ;
#17610=ORIENTED_EDGE ( 'NONE', *, *, #14305, .T. ) ;
#17614=CARTESIAN_POINT ( 'NONE',  ( 136.9873132030510305, -3657.938829547328169, 2239.009999999999764 ) ) ;
#17633=ORIENTED_EDGE ( 'NONE', *, *, #15866, .T. ) ;
#17679=ORIENTED_EDGE ( 'NONE', *, *, #2702, .T. ) ;
#17729=AXIS2_PLACEMENT_3D ( 'NONE', #16605, #1855, #554 ) ;
#17758=CARTESIAN_POINT ( 'NONE',  ( 139.6999999999999886, -3659.504999999999654, 2270.760000000000218 ) ) ;
#17782=VECTOR ( 'NONE', #17089, 1000.000000000000114 ) ;
#17787=ORIENTED_EDGE ( 'NONE', *, *, #1628, .F. ) ;
#17808=CARTESIAN_POINT ( 'NONE',  ( 142.0316867972038608, -3660.851200000135123, 2239.167815367293770 ) ) ;
#17825=AXIS2_PLACEMENT_3D ( 'NONE', #12610, #16234, #7219 ) ;
#17842=CARTESIAN_POINT ( 'NONE',  ( 139.6999999999999886, -3654.043999999999869, 2245.359999999999673 ) ) ;
#17868=DIRECTION ( 'NONE',  ( 0.000000000000000000, 0.000000000000000000, -1.000000000000000000 ) ) ;
#17869=LINE ( 'NONE', #10835, #7438 ) ;
#17877=ADVANCED_FACE ( 'NONE', ( #11816 ), #15452, .T. ) ;
#17887=CYLINDRICAL_SURFACE ( 'NONE', #891, 0.3810000000000330345 ) ;
#17966=DIRECTION ( 'NONE',  ( 0.000000000000000000, -1.000000000000000000, 0.000000000000000000 ) ) ;
#18006=CARTESIAN_POINT ( 'NONE',  ( 139.7000000001000046, -3656.812599999999748, 2242.820000000000164 ) ) ;
#18044=CIRCLE ( 'NONE', #19551, 5.080000000000000959 ) ;
#18066=( LENGTH_UNIT ( ) NAMED_UNIT ( * ) SI_UNIT ( .MILLI., .METRE. ) );
#18108=CARTESIAN_POINT ( 'NONE',  ( 137.3683132029000262, -3658.158799999999701, 2242.820000000000164 ) ) ;
#18120=DIRECTION ( 'NONE',  ( -5.666055098014000101E-14, 3.885294924352999876E-13, -1.000000000000000000 ) ) ;
#18165=VERTEX_POINT ( 'NONE', #6703 ) ;
#18199=VERTEX_POINT ( 'NONE', #12196 ) ;
#18207=CARTESIAN_POINT ( 'NONE',  ( 137.3683132029000262, -3658.158799999999701, 2242.820000000000164 ) ) ;
#18210=DIRECTION ( 'NONE',  ( 2.324635735433000053E-14, 0.000000000000000000, 1.000000000000000000 ) ) ;
#18211=VECTOR ( 'NONE', #22990, 1000.000000000000000 ) ;
#18214=CARTESIAN_POINT ( 'NONE',  ( 139.6999999999999886, -3659.504999999999654, 2245.359999999999673 ) ) ;
#18215=EDGE_LOOP ( 'NONE', ( #17787, #1753, #13358, #13528 ) ) ;
#18222=AXIS2_PLACEMENT_3D ( 'NONE', #19749, #7325, #14478 ) ;
#18247=DIRECTION ( 'NONE',  ( 0.5000000000040877302, 0.8660254037820785955, 0.000000000000000000 ) ) ;
#18308=ADVANCED_FACE ( 'NONE', ( #2673 ), #911, .T. ) ;
#18316=DIRECTION ( 'NONE',  ( -2.994914837526000224E-13, 2.590196616237999979E-13, -1.000000000000000000 ) ) ;
#18317=ADVANCED_FACE ( 'NONE', ( #6210 ), #11691, .T. ) ;
#18331=ORIENTED_EDGE ( 'NONE', *, *, #20802, .T. ) ;
#18358=CARTESIAN_POINT ( 'NONE',  ( 137.3683132029000262, -3660.851200000000063, 2242.820000000000164 ) ) ;
#18359=ORIENTED_EDGE ( 'NONE', *, *, #1663, .F. ) ;
#18380=PRODUCT_DEFINITION_CONTEXT ( 'detailed design', #7232, 'design' ) ;
#18402=LINE ( 'NONE', #1247, #11329 ) ;
#18418=CARTESIAN_POINT ( 'NONE',  ( 139.6999999999999886, -3659.504999999999654, 2239.391000000000076 ) ) ;
#18456=ORIENTED_EDGE ( 'NONE', *, *, #20113, .T. ) ;
#18503=ADVANCED_FACE ( 'NONE', ( #4903 ), #8020, .T. ) ;
#18558=FACE_OUTER_BOUND ( 'NONE', #4552, .T. ) ;
#18580=FACE_OUTER_BOUND ( 'NONE', #14903, .T. ) ;
#18584=EDGE_LOOP ( 'NONE', ( #420, #13177, #19424, #10151 ) ) ;
#18599=ORIENTED_EDGE ( 'NONE', *, *, #8712, .T. ) ;
#18620=CIRCLE ( 'NONE', #16018, 3.175000000000149925 ) ;
#18664=ADVANCED_FACE ( 'NONE', ( #2317 ), #9463, .T. ) ;
#18668=CARTESIAN_POINT ( 'NONE',  ( 142.4126867972000241, -3657.938829547000296, 2239.009999999999764 ) ) ;
#18669=DIRECTION ( 'NONE',  ( 0.000000000000000000, 0.000000000000000000, 1.000000000000000000 ) ) ;
#18675=CARTESIAN_POINT ( 'NONE',  ( 139.6999999999999886, -3659.504999999999654, 2239.009999999999764 ) ) ;
#18725=ADVANCED_FACE ( 'NONE', ( #4522 ), #11549, .T. ) ;
#18851=AXIS2_PLACEMENT_3D ( 'NONE', #11182, #18210, #3794 ) ;
#18877=EDGE_CURVE ( 'NONE', #13348, #15808, #22232, .T. ) ;
#18957=ORIENTED_EDGE ( 'NONE', *, *, #19292, .F. ) ;
#18973=ORIENTED_EDGE ( 'NONE', *, *, #7301, .F. ) ;
#19016=CARTESIAN_POINT ( 'NONE',  ( 139.6999999999999886, -3659.504999999999654, 2244.978999999999814 ) ) ;
#19034=ORIENTED_EDGE ( 'NONE', *, *, #13450, .T. ) ;
#19068=VERTEX_POINT ( 'NONE', #4046 ) ;
#19180=CARTESIAN_POINT ( 'NONE',  ( 139.6999999999999886, -3662.197400000000016, 2239.391000000000076 ) ) ;
#19181=VERTEX_POINT ( 'NONE', #10204 ) ;
#19220=VECTOR ( 'NONE', #16664, 1000.000000000000114 ) ;
#19262=CARTESIAN_POINT ( 'NONE',  ( 139.6999999999999886, -3659.504999999999654, 2245.359999999999673 ) ) ;
#19292=EDGE_CURVE ( 'NONE', #2120, #1044, #4273, .T. ) ;
#19297=CIRCLE ( 'NONE', #11788, 0.3809999999999647002 ) ;
#19321=AXIS2_PLACEMENT_3D ( 'NONE', #21515, #7104, #19634 ) ;
#19324=ADVANCED_FACE ( 'NONE', ( #6153 ), #13286, .T. ) ;
#19350=AXIS2_PLACEMENT_3D ( 'NONE', #9485, #695, #14993 ) ;
#19409=DIRECTION ( 'NONE',  ( 0.000000000000000000, 0.000000000000000000, 1.000000000000000000 ) ) ;
#19412=CARTESIAN_POINT ( 'NONE',  ( 142.0316867971961869, -3658.158799999862822, 2239.167815367171897 ) ) ;
#19424=ORIENTED_EDGE ( 'NONE', *, *, #11518, .T. ) ;
#19448=DIRECTION ( 'NONE',  ( -2.324635735433000053E-14, 2.336881798971000105E-14, -1.000000000000000000 ) ) ;
#19456=CARTESIAN_POINT ( 'NONE',  ( 142.4126867972053674, -3661.071170452545175, 2239.009999999999764 ) ) ;
#19472=FACE_BOUND ( 'NONE', #12056, .T. ) ;
#19485=DIRECTION ( 'NONE',  ( 0.000000000000000000, 0.000000000000000000, -1.000000000000000000 ) ) ;
#19526=CARTESIAN_POINT ( 'NONE',  ( 142.1895021645667327, -3658.067685255029119, 2239.009999999883348 ) ) ;
#19551=AXIS2_PLACEMENT_3D ( 'NONE', #14189, #19566, #22726 ) ;
#19566=DIRECTION ( 'NONE',  ( 0.000000000000000000, -2.336881798971000105E-14, 1.000000000000000000 ) ) ;
#19573=FACE_OUTER_BOUND ( 'NONE', #7615, .T. ) ;
#19597=PLANE ( 'NONE',  #11135 ) ;
#19615=ORIENTED_EDGE ( 'NONE', *, *, #248, .F. ) ;
#19634=DIRECTION ( 'NONE',  ( 0.000000000000000000, 0.000000000000000000, -1.000000000000000000 ) ) ;
#19723=CARTESIAN_POINT ( 'NONE',  ( 136.9873132028999976, -3661.071170452878050, 2239.009999999999764 ) ) ;
#19749=CARTESIAN_POINT ( 'NONE',  ( 142.0316867971999955, -3655.466399999999794, 2242.820000000000164 ) ) ;
#19751=EDGE_CURVE ( 'NONE', #22138, #18199, #20851, .T. ) ;
#19752=EDGE_CURVE ( 'NONE', #20464, #565, #19297, .T. ) ;
#19794=DIRECTION ( 'NONE',  ( 0.000000000000000000, -1.000000000000000000, 0.000000000000000000 ) ) ;
#19910=CIRCLE ( 'NONE', #20638, 3.175000000000149925 ) ;
#19931=VERTEX_POINT ( 'NONE', #6685 ) ;
#19949=CARTESIAN_POINT ( 'NONE',  ( 139.6999999999986528, -3662.197400000082780, 2239.391000000000076 ) ) ;
#19959=ORIENTED_EDGE ( 'NONE', *, *, #248, .T. ) ;
#20042=ADVANCED_FACE ( 'NONE', ( #14523 ), #7256, .F. ) ;
#20067=SHAPE_REPRESENTATION_RELATIONSHIP ( 'NONE' , 'NONE' ,  #5332, #22185 ) ;
#20084=ORIENTED_EDGE ( 'NONE', *, *, #20262, .F. ) ;
#20113=EDGE_CURVE ( 'NONE', #2348, #8112, #17059, .T. ) ;
#20135=PLANE ( 'NONE',  #11883 ) ;
#20179=LINE ( 'NONE', #13368, #12257 ) ;
#20192=LINE ( 'NONE', #21941, #19220 ) ;
#20220=EDGE_LOOP ( 'NONE', ( #15242, #4846, #3500, #20084 ) ) ;
#20262=EDGE_CURVE ( 'NONE', #22138, #19181, #12514, .T. ) ;
#20301=EDGE_CURVE ( 'NONE', #19931, #19068, #21058, .T. ) ;
#20323=EDGE_LOOP ( 'NONE', ( #3377, #6478, #15288, #16726 ) ) ;
#20366=CARTESIAN_POINT ( 'NONE',  ( 137.3683132028983493, -3658.158799999801431, 2239.167815367335152 ) ) ;
#20378=ORIENTED_EDGE ( 'NONE', *, *, #6540, .T. ) ;
#20402=CARTESIAN_POINT ( 'NONE',  ( 139.6999999997612747, -3662.637340905137989, 2239.009999999999764 ) ) ;
#20417=ORIENTED_EDGE ( 'NONE', *, *, #14971, .F. ) ;
#20437=CARTESIAN_POINT ( 'NONE',  ( 139.6999999999999886, -3659.504999999999654, 2245.359999999999673 ) ) ;
#20464=VERTEX_POINT ( 'NONE', #2735 ) ;
#20483=CIRCLE ( 'NONE', #14143, 5.460999999999938126 ) ;
#20485=AXIS2_PLACEMENT_3D ( 'NONE', #10068, #19448, #14063 ) ;
#20538=LINE ( 'NONE', #18668, #16203 ) ;
#20609=ORIENTED_EDGE ( 'NONE', *, *, #3990, .F. ) ;
#20633=VERTEX_POINT ( 'NONE', #17614 ) ;
#20637=DIRECTION ( 'NONE',  ( 0.000000000000000000, 1.000000000000000000, 0.000000000000000000 ) ) ;
#20638=AXIS2_PLACEMENT_3D ( 'NONE', #11184, #6145, #16790 ) ;
#20687=DIRECTION ( 'NONE',  ( 0.000000000000000000, -1.000000000000000000, 0.000000000000000000 ) ) ;
#20694=CIRCLE ( 'NONE', #3877, 5.460999999999938126 ) ;
#20724=CARTESIAN_POINT ( 'NONE',  ( 144.7800000000000011, -3659.504999999999654, 2244.978999999999814 ) ) ;
#20729=ORIENTED_EDGE ( 'NONE', *, *, #21685, .F. ) ;
#20802=EDGE_CURVE ( 'NONE', #17234, #2120, #4662, .T. ) ;
#20816=DIRECTION ( 'NONE',  ( 0.000000000000000000, 1.000000000000000000, 0.000000000000000000 ) ) ;
#20831=ORIENTED_EDGE ( 'NONE', *, *, #11381, .F. ) ;
#20851=LINE ( 'NONE', #16859, #17782 ) ;
#20970=ORIENTED_EDGE ( 'NONE', *, *, #11381, .T. ) ;
#21028=VERTEX_POINT ( 'NONE', #22744 ) ;
#21058=LINE ( 'NONE', #19180, #16318 ) ;
#21078=CARTESIAN_POINT ( 'NONE',  ( 141.0563433985999779, -3657.155744320999929, 2239.391000000000076 ) ) ;
#21126=( LENGTH_UNIT ( ) NAMED_UNIT ( * ) SI_UNIT ( .MILLI., .METRE. ) );
#21127=DIRECTION ( 'NONE',  ( -2.324635735433000053E-14, 2.336881798971000105E-14, -1.000000000000000000 ) ) ;
#21147=ORIENTED_EDGE ( 'NONE', *, *, #3051, .F. ) ;
#21171=CARTESIAN_POINT ( 'NONE',  ( 145.1609999999999729, -3659.504999999999654, 2239.390999999999622 ) ) ;
#21189=DIRECTION ( 'NONE',  ( -1.000000000000000000, -2.848935406719999894E-12, 0.000000000000000000 ) ) ;
#21213=VERTEX_POINT ( 'NONE', #7713 ) ;
#21217=FACE_OUTER_BOUND ( 'NONE', #22458, .T. ) ;
#21253=CARTESIAN_POINT ( 'NONE',  ( 139.6999999999999886, -3656.329999999999472, 2245.359999999999673 ) ) ;
#21266=CARTESIAN_POINT ( 'NONE',  ( 139.6999999999999886, -3662.197400000000016, 2242.820000000000164 ) ) ;
#21294=ORIENTED_EDGE ( 'NONE', *, *, #17018, .F. ) ;
#21306=FACE_OUTER_BOUND ( 'NONE', #18215, .T. ) ;
#21384=DIRECTION ( 'NONE',  ( -2.185478394939000111E-13, 1.295098308111999954E-13, -1.000000000000000000 ) ) ;
#21395=VERTEX_POINT ( 'NONE', #8175 ) ;
#21459=CARTESIAN_POINT ( 'NONE',  ( 139.6999999999999886, -3659.504999999999654, 2239.391000000000076 ) ) ;
#21479=DIRECTION ( 'NONE',  ( -2.324635735433000053E-14, 0.000000000000000000, -1.000000000000000000 ) ) ;
#21515=CARTESIAN_POINT ( 'NONE',  ( 134.6199999999999761, -3659.504999999999654, 2244.978999999999814 ) ) ;
#21549=ORIENTED_EDGE ( 'NONE', *, *, #20262, .T. ) ;
#21585=AXIS2_PLACEMENT_3D ( 'NONE', #186, #4731, #4609 ) ;
#21612=DIRECTION ( 'NONE',  ( 2.324635735433000053E-14, 0.000000000000000000, 1.000000000000000000 ) ) ;
#21631=CARTESIAN_POINT ( 'NONE',  ( 137.3683132029000262, -3660.851200000000063, 2242.820000000000164 ) ) ;
#21685=EDGE_CURVE ( 'NONE', #11125, #3802, #7567, .T. ) ;
#21696=CARTESIAN_POINT ( 'NONE',  ( 139.6999999999999886, -3659.504999999999654, 2239.009999999999764 ) ) ;
#21701=CARTESIAN_POINT ( 'NONE',  ( 139.6999999999986528, -3662.197400000179641, 2239.167815367330604 ) ) ;
#21713=ORIENTED_EDGE ( 'NONE', *, *, #47, .F. ) ;
#21724=LINE ( 'NONE', #16336, #12907 ) ;
#21817=DIRECTION ( 'NONE',  ( 1.000000000000000000, 1.206643234470999950E-12, 0.000000000000000000 ) ) ;
#21859=DIRECTION ( 'NONE',  ( 0.000000000000000000, 2.336881798971000105E-14, -1.000000000000000000 ) ) ;
#21866=CARTESIAN_POINT ( 'NONE',  ( 136.9873132028999976, -3661.071170452999922, 2239.009999999999764 ) ) ;
#21885=AXIS2_PLACEMENT_3D ( 'NONE', #18675, #529, #22300 ) ;
#21924=DIRECTION ( 'NONE',  ( 0.000000000000000000, -1.000000000000000000, 0.000000000000000000 ) ) ;
#21941=CARTESIAN_POINT ( 'NONE',  ( 139.7000000001000046, -3656.812599999999748, 2239.391000000000076 ) ) ;
#22053=CARTESIAN_POINT ( 'NONE',  ( 139.6999999999999886, -3659.504999999999654, 2272.030000000000200 ) ) ;
#22138=VERTEX_POINT ( 'NONE', #16105 ) ;
#22185=ADVANCED_BREP_SHAPE_REPRESENTATION ( '', ( #6253, #5611 ), #6759 ) ;
#22186=ORIENTED_EDGE ( 'NONE', *, *, #5008, .T. ) ;
#22199=PLANE ( 'NONE',  #8716 ) ;
#22227=ORIENTED_EDGE ( 'NONE', *, *, #17307, .T. ) ;
#22232=CIRCLE ( 'NONE', #17002, 3.175000000000149925 ) ;
#22241=ORIENTED_EDGE ( 'NONE', *, *, #12730, .T. ) ;
#22285=AXIS2_PLACEMENT_3D ( 'NONE', #10243, #12357, #23006 ) ;
#22290=DIRECTION ( 'NONE',  ( 1.710167014410000085E-12, -1.000000000000000000, 0.000000000000000000 ) ) ;
#22292=TOROIDAL_SURFACE ( 'NONE', #20485, 5.080000000000000071, 0.3810000000000000053 ) ;
#22300=DIRECTION ( 'NONE',  ( 1.000000000000000000, 0.000000000000000000, 0.000000000000000000 ) ) ;
#22355=CARTESIAN_POINT ( 'NONE',  ( 139.7000000001000046, -3656.812599999999748, 2242.820000000000164 ) ) ;
#22458=EDGE_LOOP ( 'NONE', ( #14579, #22227, #11679, #15410, #23141 ) ) ;
#22474=DIRECTION ( 'NONE',  ( 0.000000000000000000, 0.000000000000000000, 1.000000000000000000 ) ) ;
#22507=CARTESIAN_POINT ( 'NONE',  ( 139.6999999999999886, -3659.504999999999654, 2244.978999999999814 ) ) ;
#22522=DIRECTION ( 'NONE',  ( -2.324635735433000053E-14, 2.336881798971000105E-14, -1.000000000000000000 ) ) ;
#22524=AXIS2_PLACEMENT_3D ( 'NONE', #19016, #21127, #12215 ) ;
#22598=CARTESIAN_POINT ( 'NONE',  ( 142.0316867971999955, -3660.851200000000063, 2239.391000000000076 ) ) ;
#22599=EDGE_LOOP ( 'NONE', ( #14037, #21549, #6683, #18359 ) ) ;
#22634=LINE ( 'NONE', #3189, #953 ) ;
#22696=CARTESIAN_POINT ( 'NONE',  ( 142.0316867971999955, -3660.851200000000063, 2242.820000000000164 ) ) ;
#22710=ORIENTED_EDGE ( 'NONE', *, *, #774, .F. ) ;
#22726=DIRECTION ( 'NONE',  ( -1.000000000000000000, 0.000000000000000000, 0.000000000000000000 ) ) ;
#22740=ORIENTED_EDGE ( 'NONE', *, *, #1099, .F. ) ;
#22744=CARTESIAN_POINT ( 'NONE',  ( 139.6999999999999886, -3661.409999999999400, 2272.030000000000200 ) ) ;
#22761=ORIENTED_EDGE ( 'NONE', *, *, #1099, .T. ) ;
#22906=FACE_OUTER_BOUND ( 'NONE', #7689, .T. ) ;
#22943=CARTESIAN_POINT ( 'NONE',  ( 139.7000000002931301, -3656.372659094888149, 2239.009999999999764 ) ) ;
#22959=PRODUCT_DEFINITION ( 'UNKNOWN', '', #16119, #18380 ) ;
#22990=DIRECTION ( 'NONE',  ( -1.968992327512000303E-12, 1.000000000000000000, -3.793660610075000646E-12 ) ) ;
#22992=ORIENTED_EDGE ( 'NONE', *, *, #3670, .F. ) ;
#23006=DIRECTION ( 'NONE',  ( 1.000000000000000000, 5.432398939370942693E-28, -2.324635735433000053E-14 ) ) ;
#23011=ORIENTED_EDGE ( 'NONE', *, *, #8360, .T. ) ;
#23094=( NAMED_UNIT ( * ) SI_UNIT ( $, .STERADIAN. ) SOLID_ANGLE_UNIT ( ) );
#23101=CARTESIAN_POINT ( 'NONE',  ( 137.3683132029016178, -3660.851200000195149, 2239.167815367238745 ) ) ;
#23141=ORIENTED_EDGE ( 'NONE', *, *, #11669, .F. ) ;
#23208=COLOUR_RGB('Black',0.12,0.14,0.17);
#23209=FILL_AREA_STYLE_COLOUR('',#23208);
#23210=FILL_AREA_STYLE('',(#23209));
#23211=SURFACE_STYLE_FILL_AREA(#23210);
#23212=SURFACE_SIDE_STYLE('',(#23211));
#23213=SURFACE_STYLE_USAGE(.BOTH.,#23212);
#23214=PRESENTATION_STYLE_ASSIGNMENT((#23213));
#23234=STYLED_ITEM('',(#23214),#6253);
#23237=MECHANICAL_DESIGN_GEOMETRIC_PRESENTATION_REPRESENTATION('',(#23234),#2257);
ENDSEC;
END-ISO-10303-21;
